ISO-10303-21;
HEADER;
/* Generated by software containing ST-Developer
 * from STEP Tools, Inc. (www.steptools.com) 
 */

FILE_DESCRIPTION(
/* description */ (''),
/* implementation_level */ '2;1');

FILE_NAME(
/* name */ 'Side_Block.step',
/* time_stamp */ '2026-10-23T22:30:33+06:00',
/* author */ (''),
/* organization */ (''),
/* preprocessor_version */ 'ST-DEVELOPER v20.2',
/* originating_system */ 'Autodesk Translation Framework v15.15.0.0',
/* authorisation */ '');

FILE_SCHEMA (('AUTOMOTIVE_DESIGN { 1 0 10303 214 3 1 1 }'));
ENDSEC;

DATA;
#10=MECHANICAL_DESIGN_GEOMETRIC_PRESENTATION_REPRESENTATION('',(#236),#10131);
#216=SHAPE_REPRESENTATION_RELATIONSHIP('SRR','None',#10170,#226);
#226=ADVANCED_BREP_SHAPE_REPRESENTATION('',(#246),#10122);
#236=STYLED_ITEM('',(#10247),#246);
#246=MANIFOLD_SOLID_BREP('Side_Block',#5880);
#271=FACE_BOUND('',#870,.T.);
#272=FACE_BOUND('',#874,.T.);
#330=PLANE('',#6048);
#331=PLANE('',#6049);
#332=PLANE('',#6050);
#333=PLANE('',#6051);
#334=PLANE('',#6052);
#335=PLANE('',#6053);
#336=PLANE('',#6054);
#337=PLANE('',#6055);
#338=PLANE('',#6056);
#339=PLANE('',#6057);
#340=PLANE('',#6058);
#341=PLANE('',#6059);
#342=PLANE('',#6060);
#343=PLANE('',#6061);
#344=PLANE('',#6062);
#345=PLANE('',#6063);
#346=PLANE('',#6064);
#347=PLANE('',#6065);
#348=PLANE('',#6066);
#349=PLANE('',#6067);
#350=PLANE('',#6068);
#351=PLANE('',#6069);
#352=PLANE('',#6070);
#353=PLANE('',#6071);
#354=PLANE('',#6072);
#355=PLANE('',#6073);
#485=FACE_OUTER_BOUND('',#850,.T.);
#486=FACE_OUTER_BOUND('',#851,.T.);
#487=FACE_OUTER_BOUND('',#852,.T.);
#488=FACE_OUTER_BOUND('',#853,.T.);
#489=FACE_OUTER_BOUND('',#854,.T.);
#490=FACE_OUTER_BOUND('',#855,.T.);
#491=FACE_OUTER_BOUND('',#856,.T.);
#492=FACE_OUTER_BOUND('',#857,.T.);
#493=FACE_OUTER_BOUND('',#858,.T.);
#494=FACE_OUTER_BOUND('',#859,.T.);
#495=FACE_OUTER_BOUND('',#860,.T.);
#496=FACE_OUTER_BOUND('',#861,.T.);
#497=FACE_OUTER_BOUND('',#862,.T.);
#498=FACE_OUTER_BOUND('',#863,.T.);
#499=FACE_OUTER_BOUND('',#864,.T.);
#500=FACE_OUTER_BOUND('',#865,.T.);
#501=FACE_OUTER_BOUND('',#866,.T.);
#502=FACE_OUTER_BOUND('',#867,.T.);
#503=FACE_OUTER_BOUND('',#868,.T.);
#504=FACE_OUTER_BOUND('',#869,.T.);
#505=FACE_OUTER_BOUND('',#871,.T.);
#506=FACE_OUTER_BOUND('',#872,.T.);
#507=FACE_OUTER_BOUND('',#873,.T.);
#508=FACE_OUTER_BOUND('',#875,.T.);
#509=FACE_OUTER_BOUND('',#876,.T.);
#510=FACE_OUTER_BOUND('',#877,.T.);
#511=FACE_OUTER_BOUND('',#878,.T.);
#850=EDGE_LOOP('',(#3812,#3813,#3814,#3815));
#851=EDGE_LOOP('',(#3816,#3817,#3818,#3819));
#852=EDGE_LOOP('',(#3820,#3821,#3822,#3823));
#853=EDGE_LOOP('',(#3824,#3825,#3826,#3827));
#854=EDGE_LOOP('',(#3828,#3829,#3830,#3831));
#855=EDGE_LOOP('',(#3832,#3833,#3834,#3835));
#856=EDGE_LOOP('',(#3836,#3837,#3838,#3839));
#857=EDGE_LOOP('',(#3840,#3841,#3842,#3843));
#858=EDGE_LOOP('',(#3844,#3845,#3846,#3847));
#859=EDGE_LOOP('',(#3848,#3849,#3850,#3851));
#860=EDGE_LOOP('',(#3852,#3853,#3854,#3855));
#861=EDGE_LOOP('',(#3856,#3857,#3858,#3859));
#862=EDGE_LOOP('',(#3860,#3861,#3862,#3863));
#863=EDGE_LOOP('',(#3864,#3865,#3866,#3867));
#864=EDGE_LOOP('',(#3868,#3869,#3870,#3871));
#865=EDGE_LOOP('',(#3872,#3873,#3874,#3875));
#866=EDGE_LOOP('',(#3876,#3877,#3878,#3879));
#867=EDGE_LOOP('',(#3880,#3881,#3882,#3883));
#868=EDGE_LOOP('',(#3884,#3885,#3886,#3887));
#869=EDGE_LOOP('',(#3888,#3889,#3890,#3891,#3892,#3893,#3894,#3895,#3896,
#3897,#3898,#3899));
#870=EDGE_LOOP('',(#3900));
#871=EDGE_LOOP('',(#3901,#3902,#3903,#3904));
#872=EDGE_LOOP('',(#3905,#3906,#3907,#3908));
#873=EDGE_LOOP('',(#3909,#3910,#3911,#3912,#3913,#3914,#3915,#3916,#3917,
#3918,#3919,#3920));
#874=EDGE_LOOP('',(#3921));
#875=EDGE_LOOP('',(#3922,#3923,#3924,#3925));
#876=EDGE_LOOP('',(#3926,#3927,#3928,#3929));
#877=EDGE_LOOP('',(#3930,#3931,#3932,#3933));
#878=EDGE_LOOP('',(#3934,#3935,#3936,#3937));
#1258=LINE('',#8521,#1808);
#1259=LINE('',#8526,#1809);
#1260=LINE('',#8528,#1810);
#1261=LINE('',#8530,#1811);
#1262=LINE('',#8531,#1812);
#1263=LINE('',#8534,#1813);
#1264=LINE('',#8536,#1814);
#1265=LINE('',#8537,#1815);
#1266=LINE('',#8540,#1816);
#1267=LINE('',#8542,#1817);
#1268=LINE('',#8543,#1818);
#1269=LINE('',#8546,#1819);
#1270=LINE('',#8548,#1820);
#1271=LINE('',#8549,#1821);
#1272=LINE('',#8552,#1822);
#1273=LINE('',#8554,#1823);
#1274=LINE('',#8555,#1824);
#1275=LINE('',#8558,#1825);
#1276=LINE('',#8560,#1826);
#1277=LINE('',#8561,#1827);
#1278=LINE('',#8564,#1828);
#1279=LINE('',#8566,#1829);
#1280=LINE('',#8567,#1830);
#1281=LINE('',#8570,#1831);
#1282=LINE('',#8572,#1832);
#1283=LINE('',#8573,#1833);
#1284=LINE('',#8576,#1834);
#1285=LINE('',#8578,#1835);
#1286=LINE('',#8579,#1836);
#1287=LINE('',#8582,#1837);
#1288=LINE('',#8584,#1838);
#1289=LINE('',#8585,#1839);
#1290=LINE('',#8588,#1840);
#1291=LINE('',#8590,#1841);
#1292=LINE('',#8591,#1842);
#1293=LINE('',#8593,#1843);
#1294=LINE('',#8594,#1844);
#1295=LINE('',#8597,#1845);
#1296=LINE('',#8599,#1846);
#1297=LINE('',#8600,#1847);
#1298=LINE('',#8603,#1848);
#1299=LINE('',#8604,#1849);
#1300=LINE('',#8607,#1850);
#1301=LINE('',#8608,#1851);
#1302=LINE('',#8611,#1852);
#1303=LINE('',#8612,#1853);
#1304=LINE('',#8615,#1854);
#1305=LINE('',#8616,#1855);
#1306=LINE('',#8619,#1856);
#1307=LINE('',#8620,#1857);
#1308=LINE('',#8624,#1858);
#1309=LINE('',#8626,#1859);
#1310=LINE('',#8627,#1860);
#1311=LINE('',#8630,#1861);
#1312=LINE('',#8631,#1862);
#1313=LINE('',#8633,#1863);
#1314=LINE('',#8635,#1864);
#1315=LINE('',#8637,#1865);
#1316=LINE('',#8638,#1866);
#1317=LINE('',#8640,#1867);
#1318=LINE('',#8642,#1868);
#1808=VECTOR('',#6740,3.);
#1809=VECTOR('',#6745,10.);
#1810=VECTOR('',#6746,10.);
#1811=VECTOR('',#6747,10.);
#1812=VECTOR('',#6748,10.);
#1813=VECTOR('',#6751,10.);
#1814=VECTOR('',#6752,10.);
#1815=VECTOR('',#6753,10.);
#1816=VECTOR('',#6756,10.);
#1817=VECTOR('',#6757,10.);
#1818=VECTOR('',#6758,10.);
#1819=VECTOR('',#6761,10.);
#1820=VECTOR('',#6762,10.);
#1821=VECTOR('',#6763,10.);
#1822=VECTOR('',#6766,10.);
#1823=VECTOR('',#6767,10.);
#1824=VECTOR('',#6768,10.);
#1825=VECTOR('',#6771,10.);
#1826=VECTOR('',#6772,10.);
#1827=VECTOR('',#6773,10.);
#1828=VECTOR('',#6776,10.);
#1829=VECTOR('',#6777,10.);
#1830=VECTOR('',#6778,10.);
#1831=VECTOR('',#6781,10.);
#1832=VECTOR('',#6782,10.);
#1833=VECTOR('',#6783,10.);
#1834=VECTOR('',#6786,10.);
#1835=VECTOR('',#6787,10.);
#1836=VECTOR('',#6788,10.);
#1837=VECTOR('',#6791,10.);
#1838=VECTOR('',#6792,10.);
#1839=VECTOR('',#6793,10.);
#1840=VECTOR('',#6796,10.);
#1841=VECTOR('',#6797,10.);
#1842=VECTOR('',#6798,10.);
#1843=VECTOR('',#6801,10.);
#1844=VECTOR('',#6802,10.);
#1845=VECTOR('',#6805,10.);
#1846=VECTOR('',#6806,10.);
#1847=VECTOR('',#6807,10.);
#1848=VECTOR('',#6810,10.);
#1849=VECTOR('',#6811,10.);
#1850=VECTOR('',#6814,10.);
#1851=VECTOR('',#6815,10.);
#1852=VECTOR('',#6818,10.);
#1853=VECTOR('',#6819,10.);
#1854=VECTOR('',#6822,10.);
#1855=VECTOR('',#6823,10.);
#1856=VECTOR('',#6826,10.);
#1857=VECTOR('',#6827,10.);
#1858=VECTOR('',#6832,10.);
#1859=VECTOR('',#6833,10.);
#1860=VECTOR('',#6834,10.);
#1861=VECTOR('',#6837,10.);
#1862=VECTOR('',#6838,10.);
#1863=VECTOR('',#6841,10.);
#1864=VECTOR('',#6842,10.);
#1865=VECTOR('',#6843,10.);
#1866=VECTOR('',#6844,10.);
#1867=VECTOR('',#6847,10.);
#1868=VECTOR('',#6850,10.);
#2358=CIRCLE('',#6046,3.);
#2359=CIRCLE('',#6047,3.);
#2462=VERTEX_POINT('',#8518);
#2463=VERTEX_POINT('',#8520);
#2464=VERTEX_POINT('',#8524);
#2465=VERTEX_POINT('',#8525);
#2466=VERTEX_POINT('',#8527);
#2467=VERTEX_POINT('',#8529);
#2468=VERTEX_POINT('',#8533);
#2469=VERTEX_POINT('',#8535);
#2470=VERTEX_POINT('',#8539);
#2471=VERTEX_POINT('',#8541);
#2472=VERTEX_POINT('',#8545);
#2473=VERTEX_POINT('',#8547);
#2474=VERTEX_POINT('',#8551);
#2475=VERTEX_POINT('',#8553);
#2476=VERTEX_POINT('',#8557);
#2477=VERTEX_POINT('',#8559);
#2478=VERTEX_POINT('',#8563);
#2479=VERTEX_POINT('',#8565);
#2480=VERTEX_POINT('',#8569);
#2481=VERTEX_POINT('',#8571);
#2482=VERTEX_POINT('',#8575);
#2483=VERTEX_POINT('',#8577);
#2484=VERTEX_POINT('',#8581);
#2485=VERTEX_POINT('',#8583);
#2486=VERTEX_POINT('',#8587);
#2487=VERTEX_POINT('',#8589);
#2488=VERTEX_POINT('',#8596);
#2489=VERTEX_POINT('',#8598);
#2490=VERTEX_POINT('',#8602);
#2491=VERTEX_POINT('',#8606);
#2492=VERTEX_POINT('',#8610);
#2493=VERTEX_POINT('',#8614);
#2494=VERTEX_POINT('',#8618);
#2495=VERTEX_POINT('',#8623);
#2496=VERTEX_POINT('',#8625);
#2497=VERTEX_POINT('',#8629);
#2498=VERTEX_POINT('',#8634);
#2499=VERTEX_POINT('',#8636);
#2958=EDGE_CURVE('',#2462,#2462,#2358,.T.);
#2959=EDGE_CURVE('',#2462,#2463,#1258,.T.);
#2960=EDGE_CURVE('',#2463,#2463,#2359,.T.);
#2961=EDGE_CURVE('',#2464,#2465,#1259,.T.);
#2962=EDGE_CURVE('',#2465,#2466,#1260,.T.);
#2963=EDGE_CURVE('',#2466,#2467,#1261,.T.);
#2964=EDGE_CURVE('',#2464,#2467,#1262,.T.);
#2965=EDGE_CURVE('',#2465,#2468,#1263,.T.);
#2966=EDGE_CURVE('',#2468,#2469,#1264,.T.);
#2967=EDGE_CURVE('',#2469,#2466,#1265,.T.);
#2968=EDGE_CURVE('',#2468,#2470,#1266,.T.);
#2969=EDGE_CURVE('',#2470,#2471,#1267,.T.);
#2970=EDGE_CURVE('',#2471,#2469,#1268,.T.);
#2971=EDGE_CURVE('',#2470,#2472,#1269,.T.);
#2972=EDGE_CURVE('',#2472,#2473,#1270,.T.);
#2973=EDGE_CURVE('',#2473,#2471,#1271,.T.);
#2974=EDGE_CURVE('',#2472,#2474,#1272,.T.);
#2975=EDGE_CURVE('',#2474,#2475,#1273,.T.);
#2976=EDGE_CURVE('',#2475,#2473,#1274,.T.);
#2977=EDGE_CURVE('',#2476,#2475,#1275,.T.);
#2978=EDGE_CURVE('',#2474,#2477,#1276,.T.);
#2979=EDGE_CURVE('',#2477,#2476,#1277,.T.);
#2980=EDGE_CURVE('',#2478,#2476,#1278,.T.);
#2981=EDGE_CURVE('',#2477,#2479,#1279,.T.);
#2982=EDGE_CURVE('',#2479,#2478,#1280,.T.);
#2983=EDGE_CURVE('',#2480,#2478,#1281,.T.);
#2984=EDGE_CURVE('',#2479,#2481,#1282,.T.);
#2985=EDGE_CURVE('',#2481,#2480,#1283,.T.);
#2986=EDGE_CURVE('',#2482,#2480,#1284,.T.);
#2987=EDGE_CURVE('',#2481,#2483,#1285,.T.);
#2988=EDGE_CURVE('',#2483,#2482,#1286,.T.);
#2989=EDGE_CURVE('',#2484,#2482,#1287,.T.);
#2990=EDGE_CURVE('',#2483,#2485,#1288,.T.);
#2991=EDGE_CURVE('',#2485,#2484,#1289,.T.);
#2992=EDGE_CURVE('',#2486,#2484,#1290,.T.);
#2993=EDGE_CURVE('',#2485,#2487,#1291,.T.);
#2994=EDGE_CURVE('',#2487,#2486,#1292,.T.);
#2995=EDGE_CURVE('',#2467,#2486,#1293,.T.);
#2996=EDGE_CURVE('',#2487,#2464,#1294,.T.);
#2997=EDGE_CURVE('',#2480,#2488,#1295,.T.);
#2998=EDGE_CURVE('',#2488,#2489,#1296,.T.);
#2999=EDGE_CURVE('',#2489,#2478,#1297,.T.);
#3000=EDGE_CURVE('',#2490,#2482,#1298,.T.);
#3001=EDGE_CURVE('',#2490,#2488,#1299,.T.);
#3002=EDGE_CURVE('',#2484,#2491,#1300,.T.);
#3003=EDGE_CURVE('',#2491,#2490,#1301,.T.);
#3004=EDGE_CURVE('',#2492,#2486,#1302,.T.);
#3005=EDGE_CURVE('',#2492,#2491,#1303,.T.);
#3006=EDGE_CURVE('',#2467,#2493,#1304,.T.);
#3007=EDGE_CURVE('',#2493,#2492,#1305,.T.);
#3008=EDGE_CURVE('',#2494,#2466,#1306,.T.);
#3009=EDGE_CURVE('',#2494,#2493,#1307,.T.);
#3010=EDGE_CURVE('',#2476,#2495,#1308,.T.);
#3011=EDGE_CURVE('',#2495,#2496,#1309,.T.);
#3012=EDGE_CURVE('',#2496,#2475,#1310,.T.);
#3013=EDGE_CURVE('',#2496,#2497,#1311,.T.);
#3014=EDGE_CURVE('',#2473,#2497,#1312,.T.);
#3015=EDGE_CURVE('',#2489,#2495,#1313,.T.);
#3016=EDGE_CURVE('',#2498,#2494,#1314,.T.);
#3017=EDGE_CURVE('',#2499,#2498,#1315,.T.);
#3018=EDGE_CURVE('',#2497,#2499,#1316,.T.);
#3019=EDGE_CURVE('',#2499,#2471,#1317,.T.);
#3020=EDGE_CURVE('',#2469,#2498,#1318,.T.);
#3812=ORIENTED_EDGE('',*,*,#2958,.F.);
#3813=ORIENTED_EDGE('',*,*,#2959,.T.);
#3814=ORIENTED_EDGE('',*,*,#2960,.F.);
#3815=ORIENTED_EDGE('',*,*,#2959,.F.);
#3816=ORIENTED_EDGE('',*,*,#2961,.T.);
#3817=ORIENTED_EDGE('',*,*,#2962,.T.);
#3818=ORIENTED_EDGE('',*,*,#2963,.T.);
#3819=ORIENTED_EDGE('',*,*,#2964,.F.);
#3820=ORIENTED_EDGE('',*,*,#2965,.T.);
#3821=ORIENTED_EDGE('',*,*,#2966,.T.);
#3822=ORIENTED_EDGE('',*,*,#2967,.T.);
#3823=ORIENTED_EDGE('',*,*,#2962,.F.);
#3824=ORIENTED_EDGE('',*,*,#2968,.T.);
#3825=ORIENTED_EDGE('',*,*,#2969,.T.);
#3826=ORIENTED_EDGE('',*,*,#2970,.T.);
#3827=ORIENTED_EDGE('',*,*,#2966,.F.);
#3828=ORIENTED_EDGE('',*,*,#2971,.T.);
#3829=ORIENTED_EDGE('',*,*,#2972,.T.);
#3830=ORIENTED_EDGE('',*,*,#2973,.T.);
#3831=ORIENTED_EDGE('',*,*,#2969,.F.);
#3832=ORIENTED_EDGE('',*,*,#2974,.T.);
#3833=ORIENTED_EDGE('',*,*,#2975,.T.);
#3834=ORIENTED_EDGE('',*,*,#2976,.T.);
#3835=ORIENTED_EDGE('',*,*,#2972,.F.);
#3836=ORIENTED_EDGE('',*,*,#2977,.T.);
#3837=ORIENTED_EDGE('',*,*,#2975,.F.);
#3838=ORIENTED_EDGE('',*,*,#2978,.T.);
#3839=ORIENTED_EDGE('',*,*,#2979,.T.);
#3840=ORIENTED_EDGE('',*,*,#2980,.T.);
#3841=ORIENTED_EDGE('',*,*,#2979,.F.);
#3842=ORIENTED_EDGE('',*,*,#2981,.T.);
#3843=ORIENTED_EDGE('',*,*,#2982,.T.);
#3844=ORIENTED_EDGE('',*,*,#2983,.T.);
#3845=ORIENTED_EDGE('',*,*,#2982,.F.);
#3846=ORIENTED_EDGE('',*,*,#2984,.T.);
#3847=ORIENTED_EDGE('',*,*,#2985,.T.);
#3848=ORIENTED_EDGE('',*,*,#2986,.T.);
#3849=ORIENTED_EDGE('',*,*,#2985,.F.);
#3850=ORIENTED_EDGE('',*,*,#2987,.T.);
#3851=ORIENTED_EDGE('',*,*,#2988,.T.);
#3852=ORIENTED_EDGE('',*,*,#2989,.T.);
#3853=ORIENTED_EDGE('',*,*,#2988,.F.);
#3854=ORIENTED_EDGE('',*,*,#2990,.T.);
#3855=ORIENTED_EDGE('',*,*,#2991,.T.);
#3856=ORIENTED_EDGE('',*,*,#2992,.T.);
#3857=ORIENTED_EDGE('',*,*,#2991,.F.);
#3858=ORIENTED_EDGE('',*,*,#2993,.T.);
#3859=ORIENTED_EDGE('',*,*,#2994,.T.);
#3860=ORIENTED_EDGE('',*,*,#2995,.T.);
#3861=ORIENTED_EDGE('',*,*,#2994,.F.);
#3862=ORIENTED_EDGE('',*,*,#2996,.T.);
#3863=ORIENTED_EDGE('',*,*,#2964,.T.);
#3864=ORIENTED_EDGE('',*,*,#2983,.F.);
#3865=ORIENTED_EDGE('',*,*,#2997,.T.);
#3866=ORIENTED_EDGE('',*,*,#2998,.T.);
#3867=ORIENTED_EDGE('',*,*,#2999,.T.);
#3868=ORIENTED_EDGE('',*,*,#2986,.F.);
#3869=ORIENTED_EDGE('',*,*,#3000,.F.);
#3870=ORIENTED_EDGE('',*,*,#3001,.T.);
#3871=ORIENTED_EDGE('',*,*,#2997,.F.);
#3872=ORIENTED_EDGE('',*,*,#2989,.F.);
#3873=ORIENTED_EDGE('',*,*,#3002,.T.);
#3874=ORIENTED_EDGE('',*,*,#3003,.T.);
#3875=ORIENTED_EDGE('',*,*,#3000,.T.);
#3876=ORIENTED_EDGE('',*,*,#2992,.F.);
#3877=ORIENTED_EDGE('',*,*,#3004,.F.);
#3878=ORIENTED_EDGE('',*,*,#3005,.T.);
#3879=ORIENTED_EDGE('',*,*,#3002,.F.);
#3880=ORIENTED_EDGE('',*,*,#2995,.F.);
#3881=ORIENTED_EDGE('',*,*,#3006,.T.);
#3882=ORIENTED_EDGE('',*,*,#3007,.T.);
#3883=ORIENTED_EDGE('',*,*,#3004,.T.);
#3884=ORIENTED_EDGE('',*,*,#2963,.F.);
#3885=ORIENTED_EDGE('',*,*,#3008,.F.);
#3886=ORIENTED_EDGE('',*,*,#3009,.T.);
#3887=ORIENTED_EDGE('',*,*,#3006,.F.);
#3888=ORIENTED_EDGE('',*,*,#2961,.F.);
#3889=ORIENTED_EDGE('',*,*,#2996,.F.);
#3890=ORIENTED_EDGE('',*,*,#2993,.F.);
#3891=ORIENTED_EDGE('',*,*,#2990,.F.);
#3892=ORIENTED_EDGE('',*,*,#2987,.F.);
#3893=ORIENTED_EDGE('',*,*,#2984,.F.);
#3894=ORIENTED_EDGE('',*,*,#2981,.F.);
#3895=ORIENTED_EDGE('',*,*,#2978,.F.);
#3896=ORIENTED_EDGE('',*,*,#2974,.F.);
#3897=ORIENTED_EDGE('',*,*,#2971,.F.);
#3898=ORIENTED_EDGE('',*,*,#2968,.F.);
#3899=ORIENTED_EDGE('',*,*,#2965,.F.);
#3900=ORIENTED_EDGE('',*,*,#2958,.T.);
#3901=ORIENTED_EDGE('',*,*,#2977,.F.);
#3902=ORIENTED_EDGE('',*,*,#3010,.T.);
#3903=ORIENTED_EDGE('',*,*,#3011,.T.);
#3904=ORIENTED_EDGE('',*,*,#3012,.T.);
#3905=ORIENTED_EDGE('',*,*,#2976,.F.);
#3906=ORIENTED_EDGE('',*,*,#3012,.F.);
#3907=ORIENTED_EDGE('',*,*,#3013,.T.);
#3908=ORIENTED_EDGE('',*,*,#3014,.F.);
#3909=ORIENTED_EDGE('',*,*,#3011,.F.);
#3910=ORIENTED_EDGE('',*,*,#3015,.F.);
#3911=ORIENTED_EDGE('',*,*,#2998,.F.);
#3912=ORIENTED_EDGE('',*,*,#3001,.F.);
#3913=ORIENTED_EDGE('',*,*,#3003,.F.);
#3914=ORIENTED_EDGE('',*,*,#3005,.F.);
#3915=ORIENTED_EDGE('',*,*,#3007,.F.);
#3916=ORIENTED_EDGE('',*,*,#3009,.F.);
#3917=ORIENTED_EDGE('',*,*,#3016,.F.);
#3918=ORIENTED_EDGE('',*,*,#3017,.F.);
#3919=ORIENTED_EDGE('',*,*,#3018,.F.);
#3920=ORIENTED_EDGE('',*,*,#3013,.F.);
#3921=ORIENTED_EDGE('',*,*,#2960,.T.);
#3922=ORIENTED_EDGE('',*,*,#2973,.F.);
#3923=ORIENTED_EDGE('',*,*,#3014,.T.);
#3924=ORIENTED_EDGE('',*,*,#3018,.T.);
#3925=ORIENTED_EDGE('',*,*,#3019,.T.);
#3926=ORIENTED_EDGE('',*,*,#2970,.F.);
#3927=ORIENTED_EDGE('',*,*,#3019,.F.);
#3928=ORIENTED_EDGE('',*,*,#3017,.T.);
#3929=ORIENTED_EDGE('',*,*,#3020,.F.);
#3930=ORIENTED_EDGE('',*,*,#2967,.F.);
#3931=ORIENTED_EDGE('',*,*,#3020,.T.);
#3932=ORIENTED_EDGE('',*,*,#3016,.T.);
#3933=ORIENTED_EDGE('',*,*,#3008,.T.);
#3934=ORIENTED_EDGE('',*,*,#2980,.F.);
#3935=ORIENTED_EDGE('',*,*,#2999,.F.);
#3936=ORIENTED_EDGE('',*,*,#3015,.T.);
#3937=ORIENTED_EDGE('',*,*,#3010,.F.);
#5340=CYLINDRICAL_SURFACE('',#6045,3.);
#5548=ADVANCED_FACE('',(#485),#5340,.F.);
#5549=ADVANCED_FACE('',(#486),#330,.T.);
#5550=ADVANCED_FACE('',(#487),#331,.T.);
#5551=ADVANCED_FACE('',(#488),#332,.T.);
#5552=ADVANCED_FACE('',(#489),#333,.T.);
#5553=ADVANCED_FACE('',(#490),#334,.T.);
#5554=ADVANCED_FACE('',(#491),#335,.T.);
#5555=ADVANCED_FACE('',(#492),#336,.T.);
#5556=ADVANCED_FACE('',(#493),#337,.T.);
#5557=ADVANCED_FACE('',(#494),#338,.T.);
#5558=ADVANCED_FACE('',(#495),#339,.T.);
#5559=ADVANCED_FACE('',(#496),#340,.T.);
#5560=ADVANCED_FACE('',(#497),#341,.T.);
#5561=ADVANCED_FACE('',(#498),#342,.T.);
#5562=ADVANCED_FACE('',(#499),#343,.T.);
#5563=ADVANCED_FACE('',(#500),#344,.T.);
#5564=ADVANCED_FACE('',(#501),#345,.T.);
#5565=ADVANCED_FACE('',(#502),#346,.T.);
#5566=ADVANCED_FACE('',(#503),#347,.T.);
#5567=ADVANCED_FACE('',(#504,#271),#348,.T.);
#5568=ADVANCED_FACE('',(#505),#349,.T.);
#5569=ADVANCED_FACE('',(#506),#350,.T.);
#5570=ADVANCED_FACE('',(#507,#272),#351,.F.);
#5571=ADVANCED_FACE('',(#508),#352,.T.);
#5572=ADVANCED_FACE('',(#509),#353,.T.);
#5573=ADVANCED_FACE('',(#510),#354,.T.);
#5574=ADVANCED_FACE('',(#511),#355,.T.);
#5880=CLOSED_SHELL('',(#5548,#5549,#5550,#5551,#5552,#5553,#5554,#5555,
#5556,#5557,#5558,#5559,#5560,#5561,#5562,#5563,#5564,#5565,#5566,#5567,
#5568,#5569,#5570,#5571,#5572,#5573,#5574));
#6044=AXIS2_PLACEMENT_3D('',#8516,#6734,#6735);
#6045=AXIS2_PLACEMENT_3D('',#8517,#6736,#6737);
#6046=AXIS2_PLACEMENT_3D('',#8519,#6738,#6739);
#6047=AXIS2_PLACEMENT_3D('',#8522,#6741,#6742);
#6048=AXIS2_PLACEMENT_3D('',#8523,#6743,#6744);
#6049=AXIS2_PLACEMENT_3D('',#8532,#6749,#6750);
#6050=AXIS2_PLACEMENT_3D('',#8538,#6754,#6755);
#6051=AXIS2_PLACEMENT_3D('',#8544,#6759,#6760);
#6052=AXIS2_PLACEMENT_3D('',#8550,#6764,#6765);
#6053=AXIS2_PLACEMENT_3D('',#8556,#6769,#6770);
#6054=AXIS2_PLACEMENT_3D('',#8562,#6774,#6775);
#6055=AXIS2_PLACEMENT_3D('',#8568,#6779,#6780);
#6056=AXIS2_PLACEMENT_3D('',#8574,#6784,#6785);
#6057=AXIS2_PLACEMENT_3D('',#8580,#6789,#6790);
#6058=AXIS2_PLACEMENT_3D('',#8586,#6794,#6795);
#6059=AXIS2_PLACEMENT_3D('',#8592,#6799,#6800);
#6060=AXIS2_PLACEMENT_3D('',#8595,#6803,#6804);
#6061=AXIS2_PLACEMENT_3D('',#8601,#6808,#6809);
#6062=AXIS2_PLACEMENT_3D('',#8605,#6812,#6813);
#6063=AXIS2_PLACEMENT_3D('',#8609,#6816,#6817);
#6064=AXIS2_PLACEMENT_3D('',#8613,#6820,#6821);
#6065=AXIS2_PLACEMENT_3D('',#8617,#6824,#6825);
#6066=AXIS2_PLACEMENT_3D('',#8621,#6828,#6829);
#6067=AXIS2_PLACEMENT_3D('',#8622,#6830,#6831);
#6068=AXIS2_PLACEMENT_3D('',#8628,#6835,#6836);
#6069=AXIS2_PLACEMENT_3D('',#8632,#6839,#6840);
#6070=AXIS2_PLACEMENT_3D('',#8639,#6845,#6846);
#6071=AXIS2_PLACEMENT_3D('',#8641,#6848,#6849);
#6072=AXIS2_PLACEMENT_3D('',#8643,#6851,#6852);
#6073=AXIS2_PLACEMENT_3D('',#8644,#6853,#6854);
#6734=DIRECTION('axis',(0.,0.,1.));
#6735=DIRECTION('refdir',(1.,0.,0.));
#6736=DIRECTION('center_axis',(-1.,0.,0.));
#6737=DIRECTION('ref_axis',(0.,1.,0.));
#6738=DIRECTION('center_axis',(-1.,0.,0.));
#6739=DIRECTION('ref_axis',(0.,1.,0.));
#6740=DIRECTION('',(-1.,0.,0.));
#6741=DIRECTION('center_axis',(1.,0.,0.));
#6742=DIRECTION('ref_axis',(0.,1.,0.));
#6743=DIRECTION('center_axis',(0.707106781186548,0.,0.707106781186548));
#6744=DIRECTION('ref_axis',(0.707106781186548,0.,-0.707106781186548));
#6745=DIRECTION('',(0.,1.,0.));
#6746=DIRECTION('',(-0.678598344545846,0.281084637714824,0.678598344545846));
#6747=DIRECTION('',(0.,-1.,0.));
#6748=DIRECTION('',(-0.678598344545848,0.281084637714818,0.678598344545848));
#6749=DIRECTION('center_axis',(0.707106781186549,0.499999999999999,0.499999999999999));
#6750=DIRECTION('ref_axis',(0.577350269189624,0.,-0.816496580927727));
#6751=DIRECTION('',(0.,0.707106781186548,-0.707106781186548));
#6752=DIRECTION('',(-0.678598344545845,0.678598344545848,0.281084637714821));
#6753=DIRECTION('',(0.,-0.707106781186548,0.707106781186548));
#6754=DIRECTION('center_axis',(0.707106781186549,0.707106781186546,0.));
#6755=DIRECTION('ref_axis',(0.,0.,-1.));
#6756=DIRECTION('',(0.,0.,-1.));
#6757=DIRECTION('',(-0.678598344545846,0.67859834454585,-0.281084637714816));
#6758=DIRECTION('',(0.,0.,1.));
#6759=DIRECTION('center_axis',(0.707106781186548,0.5,-0.5));
#6760=DIRECTION('ref_axis',(-0.577350269189625,0.,-0.816496580927726));
#6761=DIRECTION('',(0.,-0.707106781186548,-0.707106781186548));
#6762=DIRECTION('',(-0.678598344545847,0.281084637714819,-0.678598344545847));
#6763=DIRECTION('',(0.,0.707106781186548,0.707106781186548));
#6764=DIRECTION('center_axis',(0.707106781186548,0.,-0.707106781186548));
#6765=DIRECTION('ref_axis',(-0.707106781186548,0.,-0.707106781186548));
#6766=DIRECTION('',(0.,-1.,0.));
#6767=DIRECTION('',(-0.678598344545847,-0.281084637714822,-0.678598344545847));
#6768=DIRECTION('',(0.,1.,0.));
#6769=DIRECTION('center_axis',(0.707106781186548,-0.499999999999999,-0.500000000000001));
#6770=DIRECTION('ref_axis',(-0.577350269189627,0.,-0.816496580927725));
#6771=DIRECTION('',(0.,0.707106781186549,-0.707106781186546));
#6772=DIRECTION('',(0.,-0.707106781186549,0.707106781186546));
#6773=DIRECTION('',(-0.678598344545845,-0.678598344545848,-0.281084637714821));
#6774=DIRECTION('center_axis',(0.707106781186549,-0.707106781186546,0.));
#6775=DIRECTION('ref_axis',(0.,0.,-1.));
#6776=DIRECTION('',(0.,0.,-1.));
#6777=DIRECTION('',(0.,0.,1.));
#6778=DIRECTION('',(-0.678598344545846,-0.678598344545848,0.281084637714821));
#6779=DIRECTION('center_axis',(0.707106781186548,-0.499999999999999,0.500000000000001));
#6780=DIRECTION('ref_axis',(0.577350269189627,0.,-0.816496580927725));
#6781=DIRECTION('',(0.,-0.707106781186549,-0.707106781186546));
#6782=DIRECTION('',(0.,0.707106781186549,0.707106781186546));
#6783=DIRECTION('',(-0.678598344545847,-0.281084637714822,0.678598344545847));
#6784=DIRECTION('center_axis',(0.707106781186548,0.,0.707106781186548));
#6785=DIRECTION('ref_axis',(0.707106781186548,0.,-0.707106781186548));
#6786=DIRECTION('',(0.,-1.,0.));
#6787=DIRECTION('',(0.,1.,0.));
#6788=DIRECTION('',(-0.678598344545848,0.281084637714818,0.678598344545848));
#6789=DIRECTION('center_axis',(0.707106781186547,0.499999999999999,0.500000000000001));
#6790=DIRECTION('ref_axis',(0.577350269189627,0.,-0.816496580927725));
#6791=DIRECTION('',(0.,-0.707106781186549,0.707106781186546));
#6792=DIRECTION('',(0.,0.707106781186549,-0.707106781186546));
#6793=DIRECTION('',(-0.678598344545847,0.678598344545849,0.281084637714816));
#6794=DIRECTION('center_axis',(0.707106781186549,0.707106781186546,0.));
#6795=DIRECTION('ref_axis',(0.,0.,-1.));
#6796=DIRECTION('',(0.,0.,1.));
#6797=DIRECTION('',(0.,0.,-1.));
#6798=DIRECTION('',(-0.678598344545847,0.678598344545849,0.281084637714816));
#6799=DIRECTION('center_axis',(0.707106781186547,0.5,0.500000000000001));
#6800=DIRECTION('ref_axis',(0.577350269189627,0.,-0.816496580927726));
#6801=DIRECTION('',(0.,-0.707106781186548,0.707106781186547));
#6802=DIRECTION('',(0.,0.707106781186548,-0.707106781186547));
#6803=DIRECTION('center_axis',(0.,-0.707106781186546,0.707106781186549));
#6804=DIRECTION('ref_axis',(1.,0.,0.));
#6805=DIRECTION('',(-1.,0.,0.));
#6806=DIRECTION('',(0.,-0.707106781186549,-0.707106781186546));
#6807=DIRECTION('',(1.,0.,0.));
#6808=DIRECTION('center_axis',(0.,0.,1.));
#6809=DIRECTION('ref_axis',(0.,-1.,0.));
#6810=DIRECTION('',(1.,0.,0.));
#6811=DIRECTION('',(0.,-1.,0.));
#6812=DIRECTION('center_axis',(0.,0.707106781186546,0.707106781186549));
#6813=DIRECTION('ref_axis',(1.,0.,0.));
#6814=DIRECTION('',(-1.,0.,0.));
#6815=DIRECTION('',(0.,-0.707106781186549,0.707106781186546));
#6816=DIRECTION('center_axis',(0.,1.,0.));
#6817=DIRECTION('ref_axis',(0.,0.,1.));
#6818=DIRECTION('',(1.,0.,0.));
#6819=DIRECTION('',(0.,0.,1.));
#6820=DIRECTION('center_axis',(0.,0.707106781186547,0.707106781186548));
#6821=DIRECTION('ref_axis',(1.,0.,0.));
#6822=DIRECTION('',(-1.,0.,0.));
#6823=DIRECTION('',(0.,-0.707106781186548,0.707106781186547));
#6824=DIRECTION('center_axis',(0.,0.,1.));
#6825=DIRECTION('ref_axis',(0.,-1.,0.));
#6826=DIRECTION('',(1.,0.,0.));
#6827=DIRECTION('',(0.,-1.,0.));
#6828=DIRECTION('center_axis',(1.,0.,0.));
#6829=DIRECTION('ref_axis',(0.,0.,-1.));
#6830=DIRECTION('center_axis',(0.,-0.707106781186546,-0.707106781186549));
#6831=DIRECTION('ref_axis',(-1.,0.,0.));
#6832=DIRECTION('',(-1.,0.,0.));
#6833=DIRECTION('',(0.,0.707106781186549,-0.707106781186546));
#6834=DIRECTION('',(1.,0.,0.));
#6835=DIRECTION('center_axis',(0.,0.,-1.));
#6836=DIRECTION('ref_axis',(0.,1.,0.));
#6837=DIRECTION('',(0.,1.,0.));
#6838=DIRECTION('',(-1.,0.,0.));
#6839=DIRECTION('center_axis',(1.,0.,0.));
#6840=DIRECTION('ref_axis',(0.,1.,0.));
#6841=DIRECTION('',(0.,0.,-1.));
#6842=DIRECTION('',(0.,-0.707106781186548,0.707106781186548));
#6843=DIRECTION('',(0.,0.,1.));
#6844=DIRECTION('',(0.,0.707106781186548,0.707106781186548));
#6845=DIRECTION('center_axis',(0.,0.707106781186548,-0.707106781186548));
#6846=DIRECTION('ref_axis',(-1.,0.,0.));
#6847=DIRECTION('',(1.,0.,0.));
#6848=DIRECTION('center_axis',(0.,1.,0.));
#6849=DIRECTION('ref_axis',(0.,0.,1.));
#6850=DIRECTION('',(-1.,0.,0.));
#6851=DIRECTION('center_axis',(0.,0.707106781186548,0.707106781186548));
#6852=DIRECTION('ref_axis',(1.,0.,0.));
#6853=DIRECTION('center_axis',(0.,-1.,0.));
#6854=DIRECTION('ref_axis',(0.,0.,-1.));
#8516=CARTESIAN_POINT('',(0.,0.,0.));
#8517=CARTESIAN_POINT('Origin',(61.,-6.90286596077709,56.9950844505733));
#8518=CARTESIAN_POINT('',(61.,-9.90286596077709,56.9950844505733));
#8519=CARTESIAN_POINT('Origin',(61.,-6.90286596077709,56.9950844505733));
#8520=CARTESIAN_POINT('',(50.,-9.90286596077709,56.9950844505733));
#8521=CARTESIAN_POINT('',(61.,-9.90286596077709,56.9950844505733));
#8522=CARTESIAN_POINT('Origin',(50.,-6.90286596077709,56.9950844505733));
#8523=CARTESIAN_POINT('Origin',(60.5,18.8741278186466,61.5));
#8524=CARTESIAN_POINT('',(61.,6.45991425627347,61.));
#8525=CARTESIAN_POINT('',(61.,28.4599142562735,61.));
#8526=CARTESIAN_POINT('',(61.,18.8741278186466,61.));
#8527=CARTESIAN_POINT('',(60.,28.8741278186466,62.));
#8528=CARTESIAN_POINT('',(61.,28.4599142562735,61.));
#8529=CARTESIAN_POINT('',(60.,6.87412781864656,62.));
#8530=CARTESIAN_POINT('',(60.,18.8741278186466,62.));
#8531=CARTESIAN_POINT('',(61.,6.45991425627347,61.));
#8532=CARTESIAN_POINT('Origin',(60.5,24.5205744280533,65.6464466094067));
#8533=CARTESIAN_POINT('',(61.,28.8741278186466,60.5857864376269));
#8534=CARTESIAN_POINT('',(61.,24.16702103746,65.2928932188134));
#8535=CARTESIAN_POINT('',(60.,29.8741278186466,61.));
#8536=CARTESIAN_POINT('',(61.,28.8741278186466,60.5857864376269));
#8537=CARTESIAN_POINT('',(60.,24.8741278186466,66.));
#8538=CARTESIAN_POINT('Origin',(60.5,29.3741278186466,54.));
#8539=CARTESIAN_POINT('',(61.,28.8741278186466,51.4142135623731));
#8540=CARTESIAN_POINT('',(61.,28.8741278186466,54.));
#8541=CARTESIAN_POINT('',(60.,29.8741278186466,51.));
#8542=CARTESIAN_POINT('',(61.,28.8741278186466,51.4142135623731));
#8543=CARTESIAN_POINT('',(60.,29.8741278186466,54.));
#8544=CARTESIAN_POINT('Origin',(60.5,25.5205744280533,47.3535533905933));
#8545=CARTESIAN_POINT('',(61.,28.4599142562735,51.));
#8546=CARTESIAN_POINT('',(61.,25.16702103746,47.7071067811865));
#8547=CARTESIAN_POINT('',(60.,28.8741278186466,50.));
#8548=CARTESIAN_POINT('',(61.,28.4599142562735,51.));
#8549=CARTESIAN_POINT('',(60.,25.8741278186466,47.));
#8550=CARTESIAN_POINT('Origin',(60.5,-3.12587218135344,50.5));
#8551=CARTESIAN_POINT('',(61.,-12.7116586189803,51.));
#8552=CARTESIAN_POINT('',(61.,-3.12587218135344,51.));
#8553=CARTESIAN_POINT('',(60.,-13.1258721813534,50.));
#8554=CARTESIAN_POINT('',(61.,-12.7116586189803,51.));
#8555=CARTESIAN_POINT('',(60.,-3.12587218135344,50.));
#8556=CARTESIAN_POINT('Origin',(60.5,-9.77231879076014,47.3535533905933));
#8557=CARTESIAN_POINT('',(60.,-14.1258721813534,51.));
#8558=CARTESIAN_POINT('',(60.,-10.1258721813534,47.));
#8559=CARTESIAN_POINT('',(61.,-13.1258721813534,51.4142135623731));
#8560=CARTESIAN_POINT('',(61.,-9.41876540016687,47.7071067811865));
#8561=CARTESIAN_POINT('',(61.,-13.1258721813534,51.4142135623731));
#8562=CARTESIAN_POINT('Origin',(60.5,-13.6258721813534,62.));
#8563=CARTESIAN_POINT('',(60.,-14.1258721813534,65.));
#8564=CARTESIAN_POINT('',(60.,-14.1258721813534,62.));
#8565=CARTESIAN_POINT('',(61.,-13.1258721813534,64.5857864376269));
#8566=CARTESIAN_POINT('',(61.,-13.1258721813534,62.));
#8567=CARTESIAN_POINT('',(61.,-13.1258721813534,64.5857864376269));
#8568=CARTESIAN_POINT('Origin',(60.5,-9.77231879076014,68.6464466094067));
#8569=CARTESIAN_POINT('',(60.,-13.1258721813534,66.));
#8570=CARTESIAN_POINT('',(60.,-10.1258721813534,69.));
#8571=CARTESIAN_POINT('',(61.,-12.7116586189803,65.));
#8572=CARTESIAN_POINT('',(61.,-9.41876540016687,68.2928932188135));
#8573=CARTESIAN_POINT('',(61.,-12.7116586189803,65.));
#8574=CARTESIAN_POINT('Origin',(60.5,6.87412781864656,65.5));
#8575=CARTESIAN_POINT('',(60.,4.87412781864656,66.));
#8576=CARTESIAN_POINT('',(60.,6.87412781864656,66.));
#8577=CARTESIAN_POINT('',(61.,4.45991425627347,65.));
#8578=CARTESIAN_POINT('',(61.,6.87412781864656,65.));
#8579=CARTESIAN_POINT('',(61.,4.45991425627347,65.));
#8580=CARTESIAN_POINT('Origin',(60.5,7.52057442805329,62.6464466094067));
#8581=CARTESIAN_POINT('',(60.,5.87412781864656,65.));
#8582=CARTESIAN_POINT('',(60.,7.87412781864656,63.));
#8583=CARTESIAN_POINT('',(61.,4.87412781864656,64.5857864376269));
#8584=CARTESIAN_POINT('',(61.,7.16702103746002,62.2928932188135));
#8585=CARTESIAN_POINT('',(61.,4.87412781864656,64.5857864376269));
#8586=CARTESIAN_POINT('Origin',(60.5,5.37412781864656,60.));
#8587=CARTESIAN_POINT('',(60.,5.87412781864656,63.));
#8588=CARTESIAN_POINT('',(60.,5.87412781864656,60.));
#8589=CARTESIAN_POINT('',(61.,4.87412781864656,62.5857864376269));
#8590=CARTESIAN_POINT('',(61.,4.87412781864656,60.));
#8591=CARTESIAN_POINT('',(61.,4.87412781864656,62.5857864376269));
#8592=CARTESIAN_POINT('Origin',(60.5,7.52057442805329,60.6464466094067));
#8593=CARTESIAN_POINT('',(60.,7.87412781864656,61.));
#8594=CARTESIAN_POINT('',(61.,7.16702103746002,60.2928932188135));
#8595=CARTESIAN_POINT('Origin',(50.,-13.6258721813534,65.5));
#8596=CARTESIAN_POINT('',(50.,-13.1258721813534,66.));
#8597=CARTESIAN_POINT('',(50.,-13.1258721813534,66.));
#8598=CARTESIAN_POINT('',(50.,-14.1258721813534,65.));
#8599=CARTESIAN_POINT('',(50.,-10.1258721813534,69.));
#8600=CARTESIAN_POINT('',(50.,-14.1258721813534,65.));
#8601=CARTESIAN_POINT('Origin',(50.,5.87412781864656,66.));
#8602=CARTESIAN_POINT('',(50.,4.87412781864656,66.));
#8603=CARTESIAN_POINT('',(50.,4.87412781864656,66.));
#8604=CARTESIAN_POINT('',(50.,5.87412781864656,66.));
#8605=CARTESIAN_POINT('Origin',(50.,5.37412781864656,65.5));
#8606=CARTESIAN_POINT('',(50.,5.87412781864656,65.));
#8607=CARTESIAN_POINT('',(50.,5.87412781864656,65.));
#8608=CARTESIAN_POINT('',(50.,7.87412781864656,63.));
#8609=CARTESIAN_POINT('Origin',(50.,5.87412781864656,62.));
#8610=CARTESIAN_POINT('',(50.,5.87412781864656,63.));
#8611=CARTESIAN_POINT('',(50.,5.87412781864656,63.));
#8612=CARTESIAN_POINT('',(50.,5.87412781864656,50.));
#8613=CARTESIAN_POINT('Origin',(50.,6.37412781864656,62.5));
#8614=CARTESIAN_POINT('',(50.,6.87412781864656,62.));
#8615=CARTESIAN_POINT('',(50.,6.87412781864656,62.));
#8616=CARTESIAN_POINT('',(50.,7.87412781864656,61.));
#8617=CARTESIAN_POINT('Origin',(50.,29.8741278186466,62.));
#8618=CARTESIAN_POINT('',(50.,28.8741278186466,62.));
#8619=CARTESIAN_POINT('',(50.,28.8741278186466,62.));
#8620=CARTESIAN_POINT('',(50.,29.8741278186466,62.));
#8621=CARTESIAN_POINT('Origin',(61.,7.87412781864656,58.));
#8622=CARTESIAN_POINT('Origin',(50.,-13.6258721813534,50.5));
#8623=CARTESIAN_POINT('',(50.,-14.1258721813534,51.));
#8624=CARTESIAN_POINT('',(50.,-14.1258721813534,51.));
#8625=CARTESIAN_POINT('',(50.,-13.1258721813534,50.));
#8626=CARTESIAN_POINT('',(50.,-10.1258721813534,47.));
#8627=CARTESIAN_POINT('',(50.,-13.1258721813534,50.));
#8628=CARTESIAN_POINT('Origin',(50.,-14.1258721813534,50.));
#8629=CARTESIAN_POINT('',(50.,28.8741278186466,50.));
#8630=CARTESIAN_POINT('',(50.,-14.1258721813534,50.));
#8631=CARTESIAN_POINT('',(50.,28.8741278186466,50.));
#8632=CARTESIAN_POINT('Origin',(50.,7.87412781864656,58.));
#8633=CARTESIAN_POINT('',(50.,-14.1258721813534,66.));
#8634=CARTESIAN_POINT('',(50.,29.8741278186466,61.));
#8635=CARTESIAN_POINT('',(50.,24.8741278186466,66.));
#8636=CARTESIAN_POINT('',(50.,29.8741278186466,51.));
#8637=CARTESIAN_POINT('',(50.,29.8741278186466,50.));
#8638=CARTESIAN_POINT('',(50.,25.8741278186466,47.));
#8639=CARTESIAN_POINT('Origin',(50.,29.3741278186466,50.5));
#8640=CARTESIAN_POINT('',(50.,29.8741278186466,51.));
#8641=CARTESIAN_POINT('Origin',(50.,29.8741278186466,50.));
#8642=CARTESIAN_POINT('',(50.,29.8741278186466,61.));
#8643=CARTESIAN_POINT('Origin',(50.,29.3741278186466,61.5));
#8644=CARTESIAN_POINT('Origin',(50.,-14.1258721813534,66.));
#10110=UNCERTAINTY_MEASURE_WITH_UNIT(LENGTH_MEASURE(0.01),#10132,
'DISTANCE_ACCURACY_VALUE',
'Maximum model space distance between geometric entities at asserted c
onnectivities');
#10119=UNCERTAINTY_MEASURE_WITH_UNIT(LENGTH_MEASURE(0.01),#10132,
'DISTANCE_ACCURACY_VALUE',
'Maximum model space distance between geometric entities at asserted c
onnectivities');
#10122=(
GEOMETRIC_REPRESENTATION_CONTEXT(3)
GLOBAL_UNCERTAINTY_ASSIGNED_CONTEXT((#10110))
GLOBAL_UNIT_ASSIGNED_CONTEXT((#10132,#10134,#10135))
REPRESENTATION_CONTEXT('','3D')
);
#10131=(
GEOMETRIC_REPRESENTATION_CONTEXT(3)
GLOBAL_UNCERTAINTY_ASSIGNED_CONTEXT((#10119))
GLOBAL_UNIT_ASSIGNED_CONTEXT((#10132,#10134,#10135))
REPRESENTATION_CONTEXT('','3D')
);
#10132=(
LENGTH_UNIT()
NAMED_UNIT(*)
SI_UNIT(.MILLI.,.METRE.)
);
#10134=(
NAMED_UNIT(*)
PLANE_ANGLE_UNIT()
SI_UNIT($,.RADIAN.)
);
#10135=(
NAMED_UNIT(*)
SI_UNIT($,.STERADIAN.)
SOLID_ANGLE_UNIT()
);
#10138=SHAPE_DEFINITION_REPRESENTATION(#10149,#10170);
#10149=PRODUCT_DEFINITION_SHAPE('',$,#10182);
#10170=SHAPE_REPRESENTATION('',(#6044),#10122);
#10179=PRODUCT_DEFINITION_CONTEXT('part definition',#10214,'design');
#10182=PRODUCT_DEFINITION('Side_Block','Side_Block',#10193,#10179);
#10193=PRODUCT_DEFINITION_FORMATION('',$,#10218);
#10214=APPLICATION_CONTEXT(
'Core Data for Automotive Mechanical Design Process');
#10215=PRODUCT_CONTEXT('part definition',#10214,'mechanical');
#10218=PRODUCT('Side_Block','Side_Block',$,(#10215));
#10241=COLOUR_RGB('Dark Blue',0.08,0.2,0.34);
#10242=FILL_AREA_STYLE_COLOUR('',#10241);
#10243=FILL_AREA_STYLE('',(#10242));
#10244=SURFACE_STYLE_FILL_AREA(#10243);
#10245=SURFACE_SIDE_STYLE('',(#10244));
#10246=SURFACE_STYLE_USAGE(.BOTH.,#10245);
#10247=PRESENTATION_STYLE_ASSIGNMENT((#10246));
ENDSEC;
END-ISO-10303-21;
